ISO-10303-21;
HEADER;
/* Generated by software containing ST-Developer
 * from STEP Tools, Inc. (www.steptools.com) 
 */

FILE_DESCRIPTION(
/* description */ (''),
/* implementation_level */ '2;1');

FILE_NAME(
/* name */ 'BASE.step',
/* time_stamp */ '2026-10-06T01:16:10-07:00',
/* author */ (''),
/* organization */ (''),
/* preprocessor_version */ 'ST-DEVELOPER v20.2',
/* originating_system */ 'Autodesk Translation Framework v15.15.0.0',
/* authorisation */ '');

FILE_SCHEMA (('AUTOMOTIVE_DESIGN { 1 0 10303 214 3 1 1 }'));
ENDSEC;

DATA;
#10=MECHANICAL_DESIGN_GEOMETRIC_PRESENTATION_REPRESENTATION('',(#296),#17113);
#264=SHAPE_REPRESENTATION_RELATIONSHIP('SRR','None',#17185,#280);
#280=ADVANCED_BREP_SHAPE_REPRESENTATION('',(#330),#17092);
#296=STYLED_ITEM('',(#17298),#330);
#330=MANIFOLD_SOLID_BREP('Body1',#6016);
#346=CYLINDRICAL_SURFACE('',#6231,2.5);
#347=CYLINDRICAL_SURFACE('',#6232,2.5);
#348=CYLINDRICAL_SURFACE('',#6233,2.5);
#349=CYLINDRICAL_SURFACE('',#6234,2.5);
#350=CYLINDRICAL_SURFACE('',#6235,1.5);
#351=CYLINDRICAL_SURFACE('',#6240,1.5);
#504=FACE_BOUND('',#1372,.T.);
#505=FACE_BOUND('',#1373,.T.);
#506=FACE_BOUND('',#1377,.T.);
#507=FACE_BOUND('',#1378,.T.);
#508=FACE_BOUND('',#1379,.T.);
#509=FACE_BOUND('',#1380,.T.);
#510=FACE_BOUND('',#1384,.T.);
#511=FACE_BOUND('',#1385,.T.);
#512=FACE_BOUND('',#1386,.T.);
#513=FACE_BOUND('',#1387,.T.);
#636=CIRCLE('',#6215,1.5);
#637=CIRCLE('',#6216,1.5);
#638=CIRCLE('',#6220,2.5);
#639=CIRCLE('',#6221,2.5);
#640=CIRCLE('',#6222,2.5);
#641=CIRCLE('',#6223,2.5);
#642=CIRCLE('',#6227,2.5);
#643=CIRCLE('',#6228,2.5);
#644=CIRCLE('',#6229,2.5);
#645=CIRCLE('',#6230,2.5);
#646=CIRCLE('',#6236,1.5);
#647=CIRCLE('',#6239,1.5);
#1008=FACE_OUTER_BOUND('',#1368,.T.);
#1009=FACE_OUTER_BOUND('',#1369,.T.);
#1010=FACE_OUTER_BOUND('',#1370,.T.);
#1011=FACE_OUTER_BOUND('',#1371,.T.);
#1012=FACE_OUTER_BOUND('',#1374,.T.);
#1013=FACE_OUTER_BOUND('',#1375,.T.);
#1014=FACE_OUTER_BOUND('',#1376,.T.);
#1015=FACE_OUTER_BOUND('',#1381,.T.);
#1016=FACE_OUTER_BOUND('',#1382,.T.);
#1017=FACE_OUTER_BOUND('',#1383,.T.);
#1018=FACE_OUTER_BOUND('',#1388,.T.);
#1019=FACE_OUTER_BOUND('',#1389,.T.);
#1020=FACE_OUTER_BOUND('',#1390,.T.);
#1021=FACE_OUTER_BOUND('',#1391,.T.);
#1022=FACE_OUTER_BOUND('',#1392,.T.);
#1023=FACE_OUTER_BOUND('',#1393,.T.);
#1024=FACE_OUTER_BOUND('',#1394,.T.);
#1025=FACE_OUTER_BOUND('',#1395,.T.);
#1368=EDGE_LOOP('',(#3916,#3917,#3918,#3919));
#1369=EDGE_LOOP('',(#3920,#3921,#3922,#3923));
#1370=EDGE_LOOP('',(#3924,#3925,#3926,#3927));
#1371=EDGE_LOOP('',(#3928,#3929,#3930,#3931,#3932,#3933));
#1372=EDGE_LOOP('',(#3934));
#1373=EDGE_LOOP('',(#3935));
#1374=EDGE_LOOP('',(#3936,#3937,#3938,#3939));
#1375=EDGE_LOOP('',(#3940,#3941,#3942,#3943,#3944));
#1376=EDGE_LOOP('',(#3945,#3946,#3947,#3948));
#1377=EDGE_LOOP('',(#3949));
#1378=EDGE_LOOP('',(#3950));
#1379=EDGE_LOOP('',(#3951));
#1380=EDGE_LOOP('',(#3952));
#1381=EDGE_LOOP('',(#3953,#3954,#3955,#3956,#3957));
#1382=EDGE_LOOP('',(#3958,#3959,#3960,#3961));
#1383=EDGE_LOOP('',(#3962,#3963,#3964,#3965));
#1384=EDGE_LOOP('',(#3966));
#1385=EDGE_LOOP('',(#3967));
#1386=EDGE_LOOP('',(#3968));
#1387=EDGE_LOOP('',(#3969));
#1388=EDGE_LOOP('',(#3970,#3971,#3972,#3973));
#1389=EDGE_LOOP('',(#3974,#3975,#3976,#3977));
#1390=EDGE_LOOP('',(#3978,#3979,#3980,#3981));
#1391=EDGE_LOOP('',(#3982,#3983,#3984,#3985));
#1392=EDGE_LOOP('',(#3986,#3987,#3988,#3989));
#1393=EDGE_LOOP('',(#3990));
#1394=EDGE_LOOP('',(#3991));
#1395=EDGE_LOOP('',(#3992,#3993,#3994,#3995));
#1860=LINE('',#8882,#2221);
#1861=LINE('',#8884,#2222);
#1862=LINE('',#8886,#2223);
#1863=LINE('',#8887,#2224);
#1864=LINE('',#8890,#2225);
#1865=LINE('',#8892,#2226);
#1866=LINE('',#8893,#2227);
#1867=LINE('',#8897,#2228);
#1868=LINE('',#8898,#2229);
#1869=LINE('',#8899,#2230);
#1870=LINE('',#8903,#2231);
#1871=LINE('',#8904,#2232);
#1872=LINE('',#8906,#2233);
#1873=LINE('',#8908,#2234);
#1874=LINE('',#8909,#2235);
#1875=LINE('',#8916,#2236);
#1876=LINE('',#8918,#2237);
#1877=LINE('',#8919,#2238);
#1878=LINE('',#8921,#2239);
#1879=LINE('',#8923,#2240);
#1880=LINE('',#8933,#2241);
#1881=LINE('',#8935,#2242);
#1882=LINE('',#8946,#2243);
#1883=LINE('',#8948,#2244);
#1884=LINE('',#8950,#2245);
#1885=LINE('',#8952,#2246);
#1886=LINE('',#8956,#2247);
#1887=LINE('',#8962,#2248);
#2221=VECTOR('',#6984,100.);
#2222=VECTOR('',#6985,20.);
#2223=VECTOR('',#6986,100.);
#2224=VECTOR('',#6987,20.);
#2225=VECTOR('',#6990,8.66025403784361);
#2226=VECTOR('',#6991,90.);
#2227=VECTOR('',#6992,8.66025403784361);
#2228=VECTOR('',#6995,7.63762615826015);
#2229=VECTOR('',#6996,110.762395693);
#2230=VECTOR('',#6997,102.875644347);
#2231=VECTOR('',#7000,100.);
#2232=VECTOR('',#7001,18.4752086140694);
#2233=VECTOR('',#7002,90.);
#2234=VECTOR('',#7003,7.63762615826015);
#2235=VECTOR('',#7004,18.4752086140694);
#2236=VECTOR('',#7011,4.);
#2237=VECTOR('',#7012,100.);
#2238=VECTOR('',#7013,4.);
#2239=VECTOR('',#7016,120.);
#2240=VECTOR('',#7019,120.);
#2241=VECTOR('',#7030,110.762395693);
#2242=VECTOR('',#7033,102.875644347);
#2243=VECTOR('',#7046,2.5);
#2244=VECTOR('',#7049,2.5);
#2245=VECTOR('',#7052,2.5);
#2246=VECTOR('',#7055,2.5);
#2247=VECTOR('',#7060,1.5);
#2248=VECTOR('',#7069,1.5);
#2582=VERTEX_POINT('',#8880);
#2583=VERTEX_POINT('',#8881);
#2584=VERTEX_POINT('',#8883);
#2585=VERTEX_POINT('',#8885);
#2586=VERTEX_POINT('',#8889);
#2587=VERTEX_POINT('',#8891);
#2588=VERTEX_POINT('',#8895);
#2589=VERTEX_POINT('',#8896);
#2590=VERTEX_POINT('',#8901);
#2591=VERTEX_POINT('',#8902);
#2592=VERTEX_POINT('',#8905);
#2593=VERTEX_POINT('',#8907);
#2594=VERTEX_POINT('',#8910);
#2595=VERTEX_POINT('',#8912);
#2596=VERTEX_POINT('',#8915);
#2597=VERTEX_POINT('',#8917);
#2598=VERTEX_POINT('',#8924);
#2599=VERTEX_POINT('',#8926);
#2600=VERTEX_POINT('',#8928);
#2601=VERTEX_POINT('',#8930);
#2602=VERTEX_POINT('',#8937);
#2603=VERTEX_POINT('',#8939);
#2604=VERTEX_POINT('',#8941);
#2605=VERTEX_POINT('',#8943);
#2606=VERTEX_POINT('',#8954);
#2607=VERTEX_POINT('',#8959);
#3104=EDGE_CURVE('',#2582,#2583,#1860,.T.);
#3105=EDGE_CURVE('',#2584,#2583,#1861,.T.);
#3106=EDGE_CURVE('',#2585,#2584,#1862,.T.);
#3107=EDGE_CURVE('',#2582,#2585,#1863,.T.);
#3108=EDGE_CURVE('',#2586,#2582,#1864,.T.);
#3109=EDGE_CURVE('',#2586,#2587,#1865,.T.);
#3110=EDGE_CURVE('',#2587,#2583,#1866,.T.);
#3111=EDGE_CURVE('',#2588,#2589,#1867,.T.);
#3112=EDGE_CURVE('',#2589,#2583,#1868,.T.);
#3113=EDGE_CURVE('',#2588,#2587,#1869,.T.);
#3114=EDGE_CURVE('',#2590,#2591,#1870,.T.);
#3115=EDGE_CURVE('',#2589,#2591,#1871,.T.);
#3116=EDGE_CURVE('',#2588,#2592,#1872,.T.);
#3117=EDGE_CURVE('',#2593,#2592,#1873,.T.);
#3118=EDGE_CURVE('',#2593,#2590,#1874,.T.);
#3119=EDGE_CURVE('',#2594,#2594,#636,.T.);
#3120=EDGE_CURVE('',#2595,#2595,#637,.T.);
#3121=EDGE_CURVE('',#2590,#2596,#1875,.T.);
#3122=EDGE_CURVE('',#2596,#2597,#1876,.T.);
#3123=EDGE_CURVE('',#2597,#2591,#1877,.T.);
#3124=EDGE_CURVE('',#2584,#2597,#1878,.T.);
#3125=EDGE_CURVE('',#2585,#2596,#1879,.T.);
#3126=EDGE_CURVE('',#2598,#2598,#638,.T.);
#3127=EDGE_CURVE('',#2599,#2599,#639,.T.);
#3128=EDGE_CURVE('',#2600,#2600,#640,.T.);
#3129=EDGE_CURVE('',#2601,#2601,#641,.T.);
#3130=EDGE_CURVE('',#2593,#2582,#1880,.T.);
#3131=EDGE_CURVE('',#2592,#2586,#1881,.T.);
#3132=EDGE_CURVE('',#2602,#2602,#642,.T.);
#3133=EDGE_CURVE('',#2603,#2603,#643,.T.);
#3134=EDGE_CURVE('',#2604,#2604,#644,.T.);
#3135=EDGE_CURVE('',#2605,#2605,#645,.T.);
#3136=EDGE_CURVE('',#2598,#2602,#1882,.T.);
#3137=EDGE_CURVE('',#2599,#2603,#1883,.T.);
#3138=EDGE_CURVE('',#2600,#2604,#1884,.T.);
#3139=EDGE_CURVE('',#2601,#2605,#1885,.T.);
#3140=EDGE_CURVE('',#2606,#2606,#646,.T.);
#3141=EDGE_CURVE('',#2606,#2594,#1886,.T.);
#3142=EDGE_CURVE('',#2607,#2607,#647,.T.);
#3143=EDGE_CURVE('',#2607,#2595,#1887,.T.);
#3916=ORIENTED_EDGE('',*,*,#3104,.T.);
#3917=ORIENTED_EDGE('',*,*,#3105,.F.);
#3918=ORIENTED_EDGE('',*,*,#3106,.F.);
#3919=ORIENTED_EDGE('',*,*,#3107,.F.);
#3920=ORIENTED_EDGE('',*,*,#3104,.F.);
#3921=ORIENTED_EDGE('',*,*,#3108,.F.);
#3922=ORIENTED_EDGE('',*,*,#3109,.T.);
#3923=ORIENTED_EDGE('',*,*,#3110,.T.);
#3924=ORIENTED_EDGE('',*,*,#3111,.T.);
#3925=ORIENTED_EDGE('',*,*,#3112,.T.);
#3926=ORIENTED_EDGE('',*,*,#3110,.F.);
#3927=ORIENTED_EDGE('',*,*,#3113,.F.);
#3928=ORIENTED_EDGE('',*,*,#3114,.T.);
#3929=ORIENTED_EDGE('',*,*,#3115,.F.);
#3930=ORIENTED_EDGE('',*,*,#3111,.F.);
#3931=ORIENTED_EDGE('',*,*,#3116,.T.);
#3932=ORIENTED_EDGE('',*,*,#3117,.F.);
#3933=ORIENTED_EDGE('',*,*,#3118,.T.);
#3934=ORIENTED_EDGE('',*,*,#3119,.F.);
#3935=ORIENTED_EDGE('',*,*,#3120,.F.);
#3936=ORIENTED_EDGE('',*,*,#3114,.F.);
#3937=ORIENTED_EDGE('',*,*,#3121,.T.);
#3938=ORIENTED_EDGE('',*,*,#3122,.T.);
#3939=ORIENTED_EDGE('',*,*,#3123,.T.);
#3940=ORIENTED_EDGE('',*,*,#3115,.T.);
#3941=ORIENTED_EDGE('',*,*,#3123,.F.);
#3942=ORIENTED_EDGE('',*,*,#3124,.F.);
#3943=ORIENTED_EDGE('',*,*,#3105,.T.);
#3944=ORIENTED_EDGE('',*,*,#3112,.F.);
#3945=ORIENTED_EDGE('',*,*,#3106,.T.);
#3946=ORIENTED_EDGE('',*,*,#3124,.T.);
#3947=ORIENTED_EDGE('',*,*,#3122,.F.);
#3948=ORIENTED_EDGE('',*,*,#3125,.F.);
#3949=ORIENTED_EDGE('',*,*,#3126,.T.);
#3950=ORIENTED_EDGE('',*,*,#3127,.T.);
#3951=ORIENTED_EDGE('',*,*,#3128,.T.);
#3952=ORIENTED_EDGE('',*,*,#3129,.T.);
#3953=ORIENTED_EDGE('',*,*,#3118,.F.);
#3954=ORIENTED_EDGE('',*,*,#3130,.T.);
#3955=ORIENTED_EDGE('',*,*,#3107,.T.);
#3956=ORIENTED_EDGE('',*,*,#3125,.T.);
#3957=ORIENTED_EDGE('',*,*,#3121,.F.);
#3958=ORIENTED_EDGE('',*,*,#3117,.T.);
#3959=ORIENTED_EDGE('',*,*,#3131,.T.);
#3960=ORIENTED_EDGE('',*,*,#3108,.T.);
#3961=ORIENTED_EDGE('',*,*,#3130,.F.);
#3962=ORIENTED_EDGE('',*,*,#3116,.F.);
#3963=ORIENTED_EDGE('',*,*,#3113,.T.);
#3964=ORIENTED_EDGE('',*,*,#3109,.F.);
#3965=ORIENTED_EDGE('',*,*,#3131,.F.);
#3966=ORIENTED_EDGE('',*,*,#3132,.F.);
#3967=ORIENTED_EDGE('',*,*,#3133,.F.);
#3968=ORIENTED_EDGE('',*,*,#3134,.F.);
#3969=ORIENTED_EDGE('',*,*,#3135,.F.);
#3970=ORIENTED_EDGE('',*,*,#3126,.F.);
#3971=ORIENTED_EDGE('',*,*,#3136,.T.);
#3972=ORIENTED_EDGE('',*,*,#3132,.T.);
#3973=ORIENTED_EDGE('',*,*,#3136,.F.);
#3974=ORIENTED_EDGE('',*,*,#3127,.F.);
#3975=ORIENTED_EDGE('',*,*,#3137,.T.);
#3976=ORIENTED_EDGE('',*,*,#3133,.T.);
#3977=ORIENTED_EDGE('',*,*,#3137,.F.);
#3978=ORIENTED_EDGE('',*,*,#3128,.F.);
#3979=ORIENTED_EDGE('',*,*,#3138,.T.);
#3980=ORIENTED_EDGE('',*,*,#3134,.T.);
#3981=ORIENTED_EDGE('',*,*,#3138,.F.);
#3982=ORIENTED_EDGE('',*,*,#3129,.F.);
#3983=ORIENTED_EDGE('',*,*,#3139,.T.);
#3984=ORIENTED_EDGE('',*,*,#3135,.T.);
#3985=ORIENTED_EDGE('',*,*,#3139,.F.);
#3986=ORIENTED_EDGE('',*,*,#3140,.F.);
#3987=ORIENTED_EDGE('',*,*,#3141,.T.);
#3988=ORIENTED_EDGE('',*,*,#3119,.T.);
#3989=ORIENTED_EDGE('',*,*,#3141,.F.);
#3990=ORIENTED_EDGE('',*,*,#3140,.T.);
#3991=ORIENTED_EDGE('',*,*,#3142,.T.);
#3992=ORIENTED_EDGE('',*,*,#3142,.F.);
#3993=ORIENTED_EDGE('',*,*,#3143,.T.);
#3994=ORIENTED_EDGE('',*,*,#3120,.T.);
#3995=ORIENTED_EDGE('',*,*,#3143,.F.);
#5504=PLANE('',#6211);
#5505=PLANE('',#6212);
#5506=PLANE('',#6213);
#5507=PLANE('',#6214);
#5508=PLANE('',#6217);
#5509=PLANE('',#6218);
#5510=PLANE('',#6219);
#5511=PLANE('',#6224);
#5512=PLANE('',#6225);
#5513=PLANE('',#6226);
#5514=PLANE('',#6237);
#5515=PLANE('',#6238);
#5656=ADVANCED_FACE('',(#1008),#5504,.F.);
#5657=ADVANCED_FACE('',(#1009),#5505,.T.);
#5658=ADVANCED_FACE('',(#1010),#5506,.T.);
#5659=ADVANCED_FACE('',(#1011,#504,#505),#5507,.F.);
#5660=ADVANCED_FACE('',(#1012),#5508,.T.);
#5661=ADVANCED_FACE('',(#1013),#5509,.T.);
#5662=ADVANCED_FACE('',(#1014,#506,#507,#508,#509),#5510,.T.);
#5663=ADVANCED_FACE('',(#1015),#5511,.T.);
#5664=ADVANCED_FACE('',(#1016),#5512,.T.);
#5665=ADVANCED_FACE('',(#1017,#510,#511,#512,#513),#5513,.T.);
#5666=ADVANCED_FACE('',(#1018),#346,.F.);
#5667=ADVANCED_FACE('',(#1019),#347,.F.);
#5668=ADVANCED_FACE('',(#1020),#348,.F.);
#5669=ADVANCED_FACE('',(#1021),#349,.F.);
#5670=ADVANCED_FACE('',(#1022),#350,.F.);
#5671=ADVANCED_FACE('',(#1023),#5514,.T.);
#5672=ADVANCED_FACE('',(#1024),#5515,.T.);
#5673=ADVANCED_FACE('',(#1025),#351,.F.);
#6016=CLOSED_SHELL('',(#5656,#5657,#5658,#5659,#5660,#5661,#5662,#5663,
#5664,#5665,#5666,#5667,#5668,#5669,#5670,#5671,#5672,#5673));
#6210=AXIS2_PLACEMENT_3D('',#8878,#6980,#6981);
#6211=AXIS2_PLACEMENT_3D('',#8879,#6982,#6983);
#6212=AXIS2_PLACEMENT_3D('',#8888,#6988,#6989);
#6213=AXIS2_PLACEMENT_3D('',#8894,#6993,#6994);
#6214=AXIS2_PLACEMENT_3D('',#8900,#6998,#6999);
#6215=AXIS2_PLACEMENT_3D('',#8911,#7005,#7006);
#6216=AXIS2_PLACEMENT_3D('',#8913,#7007,#7008);
#6217=AXIS2_PLACEMENT_3D('',#8914,#7009,#7010);
#6218=AXIS2_PLACEMENT_3D('',#8920,#7014,#7015);
#6219=AXIS2_PLACEMENT_3D('',#8922,#7017,#7018);
#6220=AXIS2_PLACEMENT_3D('',#8925,#7020,#7021);
#6221=AXIS2_PLACEMENT_3D('',#8927,#7022,#7023);
#6222=AXIS2_PLACEMENT_3D('',#8929,#7024,#7025);
#6223=AXIS2_PLACEMENT_3D('',#8931,#7026,#7027);
#6224=AXIS2_PLACEMENT_3D('',#8932,#7028,#7029);
#6225=AXIS2_PLACEMENT_3D('',#8934,#7031,#7032);
#6226=AXIS2_PLACEMENT_3D('',#8936,#7034,#7035);
#6227=AXIS2_PLACEMENT_3D('',#8938,#7036,#7037);
#6228=AXIS2_PLACEMENT_3D('',#8940,#7038,#7039);
#6229=AXIS2_PLACEMENT_3D('',#8942,#7040,#7041);
#6230=AXIS2_PLACEMENT_3D('',#8944,#7042,#7043);
#6231=AXIS2_PLACEMENT_3D('',#8945,#7044,#7045);
#6232=AXIS2_PLACEMENT_3D('',#8947,#7047,#7048);
#6233=AXIS2_PLACEMENT_3D('',#8949,#7050,#7051);
#6234=AXIS2_PLACEMENT_3D('',#8951,#7053,#7054);
#6235=AXIS2_PLACEMENT_3D('',#8953,#7056,#7057);
#6236=AXIS2_PLACEMENT_3D('',#8955,#7058,#7059);
#6237=AXIS2_PLACEMENT_3D('',#8957,#7061,#7062);
#6238=AXIS2_PLACEMENT_3D('',#8958,#7063,#7064);
#6239=AXIS2_PLACEMENT_3D('',#8960,#7065,#7066);
#6240=AXIS2_PLACEMENT_3D('',#8961,#7067,#7068);
#6980=DIRECTION('axis',(0.,0.,1.));
#6981=DIRECTION('refdir',(1.,0.,0.));
#6982=DIRECTION('center_axis',(0.,0.,1.));
#6983=DIRECTION('ref_axis',(1.,0.,0.));
#6984=DIRECTION('',(1.,0.,0.));
#6985=DIRECTION('',(0.,1.,0.));
#6986=DIRECTION('',(1.,0.,0.));
#6987=DIRECTION('',(0.,-1.,0.));
#6988=DIRECTION('center_axis',(0.,0.707106781186548,-0.707106781186548));
#6989=DIRECTION('ref_axis',(0.,0.707106781186548,0.707106781186548));
#6990=DIRECTION('',(-0.577350269189626,-0.577350269189626,-0.577350269189626));
#6991=DIRECTION('',(1.,0.,0.));
#6992=DIRECTION('',(0.577350269189626,-0.577350269189626,-0.577350269189626));
#6993=DIRECTION('center_axis',(0.707106781186548,0.707106781186548,0.));
#6994=DIRECTION('ref_axis',(0.707106781186548,-0.707106781186548,0.));
#6995=DIRECTION('',(0.654653670707987,-0.654653670707987,0.377964473009193));
#6996=DIRECTION('',(0.,0.,-1.));
#6997=DIRECTION('',(0.,0.,-1.));
#6998=DIRECTION('center_axis',(0.,-0.500000000000017,-0.866025403784429));
#6999=DIRECTION('ref_axis',(0.,0.866025403784429,-0.500000000000017));
#7000=DIRECTION('',(1.,0.,0.));
#7001=DIRECTION('',(0.,-0.866025403784429,0.500000000000017));
#7002=DIRECTION('',(-1.,0.,0.));
#7003=DIRECTION('',(0.654653670707987,0.654653670707987,-0.377964473009193));
#7004=DIRECTION('',(0.,-0.866025403784429,0.500000000000017));
#7005=DIRECTION('center_axis',(0.,0.500000000000017,0.866025403784429));
#7006=DIRECTION('ref_axis',(1.,0.,0.));
#7007=DIRECTION('center_axis',(0.,0.500000000000017,0.866025403784429));
#7008=DIRECTION('ref_axis',(1.,0.,0.));
#7009=DIRECTION('center_axis',(0.,0.,1.));
#7010=DIRECTION('ref_axis',(1.,0.,0.));
#7011=DIRECTION('',(0.,-1.,0.));
#7012=DIRECTION('',(1.,0.,0.));
#7013=DIRECTION('',(0.,1.,0.));
#7014=DIRECTION('center_axis',(1.,0.,0.));
#7015=DIRECTION('ref_axis',(0.,1.,0.));
#7016=DIRECTION('',(0.,0.,1.));
#7017=DIRECTION('center_axis',(0.,-1.,0.));
#7018=DIRECTION('ref_axis',(1.,0.,0.));
#7019=DIRECTION('',(0.,0.,1.));
#7020=DIRECTION('center_axis',(0.,1.,0.));
#7021=DIRECTION('ref_axis',(0.,0.,-1.));
#7022=DIRECTION('center_axis',(0.,1.,0.));
#7023=DIRECTION('ref_axis',(0.,0.,-1.));
#7024=DIRECTION('center_axis',(0.,1.,0.));
#7025=DIRECTION('ref_axis',(0.,0.,-1.));
#7026=DIRECTION('center_axis',(0.,1.,0.));
#7027=DIRECTION('ref_axis',(0.,0.,-1.));
#7028=DIRECTION('center_axis',(-1.,0.,0.));
#7029=DIRECTION('ref_axis',(0.,-1.,0.));
#7030=DIRECTION('',(0.,0.,-1.));
#7031=DIRECTION('center_axis',(-0.707106781186548,0.707106781186548,0.));
#7032=DIRECTION('ref_axis',(0.707106781186548,0.707106781186548,0.));
#7033=DIRECTION('',(0.,0.,-1.));
#7034=DIRECTION('center_axis',(0.,1.,0.));
#7035=DIRECTION('ref_axis',(-1.,0.,0.));
#7036=DIRECTION('center_axis',(0.,1.,0.));
#7037=DIRECTION('ref_axis',(0.,0.,-1.));
#7038=DIRECTION('center_axis',(0.,1.,0.));
#7039=DIRECTION('ref_axis',(0.,0.,-1.));
#7040=DIRECTION('center_axis',(0.,1.,0.));
#7041=DIRECTION('ref_axis',(0.,0.,-1.));
#7042=DIRECTION('center_axis',(0.,1.,0.));
#7043=DIRECTION('ref_axis',(0.,0.,-1.));
#7044=DIRECTION('center_axis',(0.,1.,0.));
#7045=DIRECTION('ref_axis',(0.,0.,-1.));
#7046=DIRECTION('',(0.,1.,0.));
#7047=DIRECTION('center_axis',(0.,1.,0.));
#7048=DIRECTION('ref_axis',(0.,0.,-1.));
#7049=DIRECTION('',(0.,1.,0.));
#7050=DIRECTION('center_axis',(0.,1.,0.));
#7051=DIRECTION('ref_axis',(0.,0.,-1.));
#7052=DIRECTION('',(0.,1.,0.));
#7053=DIRECTION('center_axis',(0.,1.,0.));
#7054=DIRECTION('ref_axis',(0.,0.,-1.));
#7055=DIRECTION('',(0.,1.,0.));
#7056=DIRECTION('center_axis',(0.,0.500000000000017,0.866025403784429));
#7057=DIRECTION('ref_axis',(1.,0.,0.));
#7058=DIRECTION('center_axis',(0.,0.500000000000017,0.866025403784429));
#7059=DIRECTION('ref_axis',(1.,0.,0.));
#7060=DIRECTION('',(0.,0.500000000000017,0.866025403784429));
#7061=DIRECTION('center_axis',(0.,0.500000000000017,0.866025403784429));
#7062=DIRECTION('ref_axis',(1.,0.,0.));
#7063=DIRECTION('center_axis',(0.,0.500000000000017,0.866025403784429));
#7064=DIRECTION('ref_axis',(1.,0.,0.));
#7065=DIRECTION('center_axis',(0.,0.500000000000017,0.866025403784429));
#7066=DIRECTION('ref_axis',(1.,0.,0.));
#7067=DIRECTION('center_axis',(0.,0.500000000000017,0.866025403784429));
#7068=DIRECTION('ref_axis',(1.,0.,0.));
#7069=DIRECTION('',(0.,0.500000000000017,0.866025403784429));
#8878=CARTESIAN_POINT('',(0.,0.,0.));
#8879=CARTESIAN_POINT('Origin',(0.,0.,-60.));
#8880=CARTESIAN_POINT('',(-50.,20.,-60.));
#8881=CARTESIAN_POINT('',(50.,20.,-60.));
#8882=CARTESIAN_POINT('',(-50.,20.,-60.));
#8883=CARTESIAN_POINT('',(50.,0.,-60.));
#8884=CARTESIAN_POINT('',(50.,0.,-60.));
#8885=CARTESIAN_POINT('',(-50.,0.,-60.));
#8886=CARTESIAN_POINT('',(-50.,0.,-60.));
#8887=CARTESIAN_POINT('',(-50.,20.,-60.));
#8888=CARTESIAN_POINT('Origin',(0.,22.5,-57.5));
#8889=CARTESIAN_POINT('',(-45.,25.,-55.));
#8890=CARTESIAN_POINT('',(-45.,25.,-55.));
#8891=CARTESIAN_POINT('',(45.,25.,-55.));
#8892=CARTESIAN_POINT('',(-45.,25.,-55.));
#8893=CARTESIAN_POINT('',(45.,25.,-55.));
#8894=CARTESIAN_POINT('Origin',(47.5,22.5,2.84217094304E-14));
#8895=CARTESIAN_POINT('',(45.,25.,47.87564434702));
#8896=CARTESIAN_POINT('',(50.,20.,50.76239569297));
#8897=CARTESIAN_POINT('',(45.,25.,47.87564434702));
#8898=CARTESIAN_POINT('',(50.,20.,50.76239569297));
#8899=CARTESIAN_POINT('',(45.,25.,47.87564434702));
#8900=CARTESIAN_POINT('Origin',(-57.3,4.,60.));
#8901=CARTESIAN_POINT('',(-50.,4.,60.));
#8902=CARTESIAN_POINT('',(50.,4.,60.));
#8903=CARTESIAN_POINT('',(-50.,4.,60.));
#8904=CARTESIAN_POINT('',(50.,20.,50.76239569297));
#8905=CARTESIAN_POINT('',(-45.,25.,47.87564434702));
#8906=CARTESIAN_POINT('',(45.,25.,47.87564434702));
#8907=CARTESIAN_POINT('',(-50.,20.,50.76239569297));
#8908=CARTESIAN_POINT('',(-50.,20.,50.76239569297));
#8909=CARTESIAN_POINT('',(-50.,20.,50.76239569297));
#8910=CARTESIAN_POINT('',(-27.5,14.17468245269,54.12564434702));
#8911=CARTESIAN_POINT('Origin',(-26.,14.17468245269,54.12564434702));
#8912=CARTESIAN_POINT('',(24.5,14.17468245269,54.12564434702));
#8913=CARTESIAN_POINT('Origin',(26.,14.17468245269,54.12564434702));
#8914=CARTESIAN_POINT('Origin',(0.,0.,60.));
#8915=CARTESIAN_POINT('',(-50.,0.,60.));
#8916=CARTESIAN_POINT('',(-50.,4.,60.));
#8917=CARTESIAN_POINT('',(50.,0.,60.));
#8918=CARTESIAN_POINT('',(-50.,0.,60.));
#8919=CARTESIAN_POINT('',(50.,0.,60.));
#8920=CARTESIAN_POINT('Origin',(50.,0.,-60.));
#8921=CARTESIAN_POINT('',(50.,0.,-60.));
#8922=CARTESIAN_POINT('Origin',(-50.,0.,-60.));
#8923=CARTESIAN_POINT('',(-50.,0.,-60.));
#8924=CARTESIAN_POINT('',(-32.5,0.,35.));
#8925=CARTESIAN_POINT('Origin',(-32.5,0.,32.5));
#8926=CARTESIAN_POINT('',(-32.5,0.,-30.));
#8927=CARTESIAN_POINT('Origin',(-32.5,0.,-32.5));
#8928=CARTESIAN_POINT('',(32.5,0.,35.));
#8929=CARTESIAN_POINT('Origin',(32.5,0.,32.5));
#8930=CARTESIAN_POINT('',(32.5,0.,-30.));
#8931=CARTESIAN_POINT('Origin',(32.5,0.,-32.5));
#8932=CARTESIAN_POINT('Origin',(-50.,25.,-60.));
#8933=CARTESIAN_POINT('',(-50.,20.,50.76239569297));
#8934=CARTESIAN_POINT('Origin',(-47.5,22.5,2.84217094304E-14));
#8935=CARTESIAN_POINT('',(-45.,25.,47.87564434702));
#8936=CARTESIAN_POINT('Origin',(50.,25.,-60.));
#8937=CARTESIAN_POINT('',(-32.5,25.,35.));
#8938=CARTESIAN_POINT('Origin',(-32.5,25.,32.5));
#8939=CARTESIAN_POINT('',(-32.5,25.,-30.));
#8940=CARTESIAN_POINT('Origin',(-32.5,25.,-32.5));
#8941=CARTESIAN_POINT('',(32.5,25.,35.));
#8942=CARTESIAN_POINT('Origin',(32.5,25.,32.5));
#8943=CARTESIAN_POINT('',(32.5,25.,-30.));
#8944=CARTESIAN_POINT('Origin',(32.5,25.,-32.5));
#8945=CARTESIAN_POINT('Origin',(-32.5,25.,32.5));
#8946=CARTESIAN_POINT('',(-32.5,25.,35.));
#8947=CARTESIAN_POINT('Origin',(-32.5,25.,-32.5));
#8948=CARTESIAN_POINT('',(-32.5,25.,-30.));
#8949=CARTESIAN_POINT('Origin',(32.5,25.,32.5));
#8950=CARTESIAN_POINT('',(32.5,25.,35.));
#8951=CARTESIAN_POINT('Origin',(32.5,25.,-32.5));
#8952=CARTESIAN_POINT('',(32.5,25.,-30.));
#8953=CARTESIAN_POINT('Origin',(-26.,14.17468245269,54.12564434702));
#8954=CARTESIAN_POINT('',(-27.5,9.17468245268864,45.4653903091737));
#8955=CARTESIAN_POINT('Origin',(-26.,9.174682452695,45.46539030917));
#8956=CARTESIAN_POINT('',(-27.5,14.17468245269,54.12564434702));
#8957=CARTESIAN_POINT('Origin',(-57.3,21.98076211353,38.07179676972));
#8958=CARTESIAN_POINT('Origin',(-57.3,21.98076211353,38.07179676972));
#8959=CARTESIAN_POINT('',(24.5,9.17468245268864,45.4653903091737));
#8960=CARTESIAN_POINT('Origin',(26.,9.174682452695,45.46539030917));
#8961=CARTESIAN_POINT('Origin',(26.,14.17468245269,54.12564434702));
#8962=CARTESIAN_POINT('',(24.5,14.17468245269,54.12564434702));
#17069=UNCERTAINTY_MEASURE_WITH_UNIT(LENGTH_MEASURE(0.01),#17114,
'DISTANCE_ACCURACY_VALUE',
'Maximum model space distance between geometric entities at asserted c
onnectivities');
#17090=UNCERTAINTY_MEASURE_WITH_UNIT(LENGTH_MEASURE(0.01),#17114,
'DISTANCE_ACCURACY_VALUE',
'Maximum model space distance between geometric entities at asserted c
onnectivities');
#17092=(
GEOMETRIC_REPRESENTATION_CONTEXT(3)
GLOBAL_UNCERTAINTY_ASSIGNED_CONTEXT((#17069))
GLOBAL_UNIT_ASSIGNED_CONTEXT((#17114,#17116,#17117))
REPRESENTATION_CONTEXT('','3D')
);
#17113=(
GEOMETRIC_REPRESENTATION_CONTEXT(3)
GLOBAL_UNCERTAINTY_ASSIGNED_CONTEXT((#17090))
GLOBAL_UNIT_ASSIGNED_CONTEXT((#17114,#17116,#17117))
REPRESENTATION_CONTEXT('','3D')
);
#17114=(
LENGTH_UNIT()
NAMED_UNIT(*)
SI_UNIT(.MILLI.,.METRE.)
);
#17116=(
NAMED_UNIT(*)
PLANE_ANGLE_UNIT()
SI_UNIT($,.RADIAN.)
);
#17117=(
NAMED_UNIT(*)
SI_UNIT($,.STERADIAN.)
SOLID_ANGLE_UNIT()
);
#17119=SHAPE_DEFINITION_REPRESENTATION(#17141,#17185);
#17141=PRODUCT_DEFINITION_SHAPE('',$,#17208);
#17185=SHAPE_REPRESENTATION('',(#6210),#17092);
#17206=PRODUCT_DEFINITION_CONTEXT('part definition',#17274,'design');
#17208=PRODUCT_DEFINITION('base','BASE',#17230,#17206);
#17230=PRODUCT_DEFINITION_FORMATION('',$,#17277);
#17274=APPLICATION_CONTEXT(
'Core Data for Automotive Mechanical Design Process');
#17275=PRODUCT_CONTEXT('part definition',#17274,'mechanical');
#17277=PRODUCT('base','BASE',$,(#17275));
#17298=PRESENTATION_STYLE_ASSIGNMENT((#17299));
#17299=SURFACE_STYLE_USAGE(.BOTH.,#17300);
#17300=SURFACE_SIDE_STYLE('',(#17301));
#17301=SURFACE_STYLE_FILL_AREA(#17302);
#17302=FILL_AREA_STYLE('Steel - Satin',(#17303));
#17303=FILL_AREA_STYLE_COLOUR('Steel - Satin',#17304);
#17304=COLOUR_RGB('Steel - Satin', 0.09019608, 0.27058824, 0.51372549);
ENDSEC;
END-ISO-10303-21;
